ISO-10303-21;
HEADER;
/* Generated by software containing ST-Developer
 * from STEP Tools, Inc. (www.steptools.com) 
 */

FILE_DESCRIPTION(
/* description */ ('Line shaft on three pillow blocks'),
/* implementation_level */ '2;1');

FILE_NAME(
/* name */ 'Shaft end disc (1).step',
/* time_stamp */ '2026-10-27T10:49:19-07:00',
/* author */ (''),
/* organization */ (''),
/* preprocessor_version */ 'ST-DEVELOPER v20.2',
/* originating_system */ 'Autodesk Translation Framework v15.17.0.0',
/* authorisation */ '');

FILE_SCHEMA (('AUTOMOTIVE_DESIGN { 1 0 10303 214 3 1 1 }'));
ENDSEC;

DATA;
#10=MECHANICAL_DESIGN_GEOMETRIC_PRESENTATION_REPRESENTATION('',(#362),#8377);
#307=SHAPE_REPRESENTATION_RELATIONSHIP('SRR','None',#8524,#334);
#334=ADVANCED_BREP_SHAPE_REPRESENTATION('',(#388),#8373);
#362=STYLED_ITEM('',(#8718),#388);
#388=MANIFOLD_SOLID_BREP('Body1',#4350);
#484=FACE_BOUND('',#1211,.T.);
#485=FACE_BOUND('',#1213,.T.);
#622=PLANE('',#5075);
#623=PLANE('',#5076);
#863=FACE_OUTER_BOUND('',#1208,.T.);
#864=FACE_OUTER_BOUND('',#1209,.T.);
#865=FACE_OUTER_BOUND('',#1210,.T.);
#866=FACE_OUTER_BOUND('',#1212,.T.);
#1208=EDGE_LOOP('',(#3827,#3828,#3829,#3830));
#1209=EDGE_LOOP('',(#3831,#3832,#3833,#3834));
#1210=EDGE_LOOP('',(#3835));
#1211=EDGE_LOOP('',(#3836));
#1212=EDGE_LOOP('',(#3837));
#1213=EDGE_LOOP('',(#3838));
#1511=LINE('',#8112,#1838);
#1512=LINE('',#8118,#1839);
#1838=VECTOR('',#6240,0.275);
#1839=VECTOR('',#6247,1.1);
#2052=CIRCLE('',#5070,0.275);
#2053=CIRCLE('',#5071,0.275);
#2054=CIRCLE('',#5073,1.1);
#2055=CIRCLE('',#5074,1.1);
#2367=VERTEX_POINT('',#8109);
#2368=VERTEX_POINT('',#8111);
#2369=VERTEX_POINT('',#8115);
#2370=VERTEX_POINT('',#8117);
#2862=EDGE_CURVE('',#2367,#2367,#2052,.T.);
#2863=EDGE_CURVE('',#2367,#2368,#1511,.T.);
#2864=EDGE_CURVE('',#2368,#2368,#2053,.T.);
#2865=EDGE_CURVE('',#2369,#2369,#2054,.T.);
#2866=EDGE_CURVE('',#2369,#2370,#1512,.T.);
#2867=EDGE_CURVE('',#2370,#2370,#2055,.T.);
#3827=ORIENTED_EDGE('',*,*,#2862,.F.);
#3828=ORIENTED_EDGE('',*,*,#2863,.T.);
#3829=ORIENTED_EDGE('',*,*,#2864,.T.);
#3830=ORIENTED_EDGE('',*,*,#2863,.F.);
#3831=ORIENTED_EDGE('',*,*,#2865,.F.);
#3832=ORIENTED_EDGE('',*,*,#2866,.T.);
#3833=ORIENTED_EDGE('',*,*,#2867,.T.);
#3834=ORIENTED_EDGE('',*,*,#2866,.F.);
#3835=ORIENTED_EDGE('',*,*,#2865,.T.);
#3836=ORIENTED_EDGE('',*,*,#2862,.T.);
#3837=ORIENTED_EDGE('',*,*,#2867,.F.);
#3838=ORIENTED_EDGE('',*,*,#2864,.F.);
#4067=CYLINDRICAL_SURFACE('',#5069,0.275);
#4068=CYLINDRICAL_SURFACE('',#5072,1.1);
#4281=ADVANCED_FACE('',(#863),#4067,.F.);
#4282=ADVANCED_FACE('',(#864),#4068,.T.);
#4283=ADVANCED_FACE('',(#865,#484),#622,.T.);
#4284=ADVANCED_FACE('',(#866,#485),#623,.F.);
#4350=CLOSED_SHELL('',(#4281,#4282,#4283,#4284));
#5068=AXIS2_PLACEMENT_3D('',#8107,#6234,#6235);
#5069=AXIS2_PLACEMENT_3D('',#8108,#6236,#6237);
#5070=AXIS2_PLACEMENT_3D('',#8110,#6238,#6239);
#5071=AXIS2_PLACEMENT_3D('',#8113,#6241,#6242);
#5072=AXIS2_PLACEMENT_3D('',#8114,#6243,#6244);
#5073=AXIS2_PLACEMENT_3D('',#8116,#6245,#6246);
#5074=AXIS2_PLACEMENT_3D('',#8119,#6248,#6249);
#5075=AXIS2_PLACEMENT_3D('',#8120,#6250,#6251);
#5076=AXIS2_PLACEMENT_3D('',#8121,#6252,#6253);
#6234=DIRECTION('axis',(0.,0.,1.));
#6235=DIRECTION('refdir',(1.,0.,0.));
#6236=DIRECTION('center_axis',(0.,1.,0.));
#6237=DIRECTION('ref_axis',(1.,0.,0.));
#6238=DIRECTION('center_axis',(0.,-1.,0.));
#6239=DIRECTION('ref_axis',(1.,0.,0.));
#6240=DIRECTION('',(0.,-1.,0.));
#6241=DIRECTION('center_axis',(0.,-1.,0.));
#6242=DIRECTION('ref_axis',(1.,0.,0.));
#6243=DIRECTION('center_axis',(0.,1.,0.));
#6244=DIRECTION('ref_axis',(1.,0.,0.));
#6245=DIRECTION('center_axis',(0.,1.,0.));
#6246=DIRECTION('ref_axis',(1.,0.,0.));
#6247=DIRECTION('',(0.,-1.,0.));
#6248=DIRECTION('center_axis',(0.,1.,0.));
#6249=DIRECTION('ref_axis',(1.,0.,0.));
#6250=DIRECTION('center_axis',(0.,1.,0.));
#6251=DIRECTION('ref_axis',(1.,0.,0.));
#6252=DIRECTION('center_axis',(0.,1.,0.));
#6253=DIRECTION('ref_axis',(1.,0.,0.));
#8107=CARTESIAN_POINT('',(0.,0.,0.));
#8108=CARTESIAN_POINT('Origin',(0.,34.5,4.53));
#8109=CARTESIAN_POINT('',(-0.275,34.7,4.53));
#8110=CARTESIAN_POINT('Origin',(0.,34.7,4.53));
#8111=CARTESIAN_POINT('',(-0.275,34.5,4.53));
#8112=CARTESIAN_POINT('',(-0.275,34.5,4.53));
#8113=CARTESIAN_POINT('Origin',(0.,34.5,4.53));
#8114=CARTESIAN_POINT('Origin',(0.,34.5,4.53));
#8115=CARTESIAN_POINT('',(-1.1,34.7,4.53));
#8116=CARTESIAN_POINT('Origin',(0.,34.7,4.53));
#8117=CARTESIAN_POINT('',(-1.1,34.5,4.53));
#8118=CARTESIAN_POINT('',(-1.1,34.5,4.53));
#8119=CARTESIAN_POINT('Origin',(0.,34.5,4.53));
#8120=CARTESIAN_POINT('Origin',(0.,34.7,4.53));
#8121=CARTESIAN_POINT('Origin',(0.,34.5,4.53));
#8341=UNCERTAINTY_MEASURE_WITH_UNIT(LENGTH_MEASURE(0.001),#8378,
'DISTANCE_ACCURACY_VALUE',
'Maximum model space distance between geometric entities at asserted c
onnectivities');
#8345=UNCERTAINTY_MEASURE_WITH_UNIT(LENGTH_MEASURE(0.001),#8378,
'DISTANCE_ACCURACY_VALUE',
'Maximum model space distance between geometric entities at asserted c
onnectivities');
#8373=(
GEOMETRIC_REPRESENTATION_CONTEXT(3)
GLOBAL_UNCERTAINTY_ASSIGNED_CONTEXT((#8341))
GLOBAL_UNIT_ASSIGNED_CONTEXT((#8378,#8380,#8381))
REPRESENTATION_CONTEXT('','3D')
);
#8377=(
GEOMETRIC_REPRESENTATION_CONTEXT(3)
GLOBAL_UNCERTAINTY_ASSIGNED_CONTEXT((#8345))
GLOBAL_UNIT_ASSIGNED_CONTEXT((#8378,#8380,#8381))
REPRESENTATION_CONTEXT('','3D')
);
#8378=(
LENGTH_UNIT()
NAMED_UNIT(*)
SI_UNIT(.CENTI.,.METRE.)
);
#8380=(
NAMED_UNIT(*)
PLANE_ANGLE_UNIT()
SI_UNIT($,.RADIAN.)
);
#8381=(
NAMED_UNIT(*)
SI_UNIT($,.STERADIAN.)
SOLID_ANGLE_UNIT()
);
#8409=SHAPE_DEFINITION_REPRESENTATION(#8476,#8524);
#8476=PRODUCT_DEFINITION_SHAPE('',$,#8556);
#8524=SHAPE_REPRESENTATION('',(#5068),#8373);
#8528=PRODUCT_DEFINITION_CONTEXT('part definition',#8623,'design');
#8556=PRODUCT_DEFINITION('Shaft end disc (1)','Shaft end disc (1)',#8587,
#8528);
#8587=PRODUCT_DEFINITION_FORMATION('',$,#8652);
#8623=APPLICATION_CONTEXT(
'Core Data for Automotive Mechanical Design Process');
#8624=PRODUCT_CONTEXT('part definition',#8623,'mechanical');
#8652=PRODUCT('Shaft end disc (1)','Shaft end disc (1)','Shaft end disc (1)',
(#8624));
#8712=COLOUR_RGB('Grey',0.48,0.52,0.57);
#8713=FILL_AREA_STYLE_COLOUR('',#8712);
#8714=FILL_AREA_STYLE('',(#8713));
#8715=SURFACE_STYLE_FILL_AREA(#8714);
#8716=SURFACE_SIDE_STYLE('',(#8715));
#8717=SURFACE_STYLE_USAGE(.BOTH.,#8716);
#8718=PRESENTATION_STYLE_ASSIGNMENT((#8717));
ENDSEC;
END-ISO-10303-21;
